ISO-10303-21;
HEADER;
/* Generated by software containing ST-Developer
 * from STEP Tools, Inc. (www.steptools.com) 
 */

FILE_DESCRIPTION(
/* description */ ('Jaw-coupled motor to shaft test stand'),
/* implementation_level */ '2;1');

FILE_NAME(
/* name */ 'M3x10 motor screw (2).step',
/* time_stamp */ '2026-10-27T10:46:06-07:00',
/* author */ (''),
/* organization */ (''),
/* preprocessor_version */ 'ST-DEVELOPER v20.2',
/* originating_system */ 'Autodesk Translation Framework v15.17.0.0',
/* authorisation */ '');

FILE_SCHEMA (('AUTOMOTIVE_DESIGN { 1 0 10303 214 3 1 1 }'));
ENDSEC;

DATA;
#10=MECHANICAL_DESIGN_GEOMETRIC_PRESENTATION_REPRESENTATION('',(#351),#19361);
#287=SHAPE_REPRESENTATION_RELATIONSHIP('SRR','None',#19501,#319);
#319=ADVANCED_BREP_SHAPE_REPRESENTATION('',(#384),#19337);
#351=STYLED_ITEM('',(#19753),#384);
#384=MANIFOLD_SOLID_BREP('Body1',#10995);
#448=FACE_BOUND('',#1791,.T.);
#449=FACE_BOUND('',#1794,.T.);
#581=PLANE('',#11545);
#582=PLANE('',#11546);
#583=PLANE('',#11547);
#584=PLANE('',#11548);
#585=PLANE('',#11549);
#586=PLANE('',#11550);
#587=PLANE('',#11551);
#588=PLANE('',#11552);
#589=PLANE('',#11557);
#590=PLANE('',#11560);
#1118=FACE_OUTER_BOUND('',#1783,.T.);
#1119=FACE_OUTER_BOUND('',#1784,.T.);
#1120=FACE_OUTER_BOUND('',#1785,.T.);
#1121=FACE_OUTER_BOUND('',#1786,.T.);
#1122=FACE_OUTER_BOUND('',#1787,.T.);
#1123=FACE_OUTER_BOUND('',#1788,.T.);
#1124=FACE_OUTER_BOUND('',#1789,.T.);
#1125=FACE_OUTER_BOUND('',#1790,.T.);
#1126=FACE_OUTER_BOUND('',#1792,.T.);
#1127=FACE_OUTER_BOUND('',#1793,.T.);
#1128=FACE_OUTER_BOUND('',#1795,.T.);
#1129=FACE_OUTER_BOUND('',#1796,.T.);
#1783=EDGE_LOOP('',(#7736,#7737,#7738,#7739));
#1784=EDGE_LOOP('',(#7740,#7741,#7742,#7743));
#1785=EDGE_LOOP('',(#7744,#7745,#7746,#7747));
#1786=EDGE_LOOP('',(#7748,#7749,#7750,#7751));
#1787=EDGE_LOOP('',(#7752,#7753,#7754,#7755));
#1788=EDGE_LOOP('',(#7756,#7757,#7758,#7759));
#1789=EDGE_LOOP('',(#7760,#7761,#7762,#7763,#7764,#7765));
#1790=EDGE_LOOP('',(#7766));
#1791=EDGE_LOOP('',(#7767));
#1792=EDGE_LOOP('',(#7768,#7769,#7770,#7771));
#1793=EDGE_LOOP('',(#7772));
#1794=EDGE_LOOP('',(#7773,#7774,#7775,#7776,#7777,#7778));
#1795=EDGE_LOOP('',(#7779,#7780,#7781,#7782));
#1796=EDGE_LOOP('',(#7783));
#2508=LINE('',#15865,#3661);
#2509=LINE('',#15867,#3662);
#2510=LINE('',#15869,#3663);
#2511=LINE('',#15870,#3664);
#2512=LINE('',#15873,#3665);
#2513=LINE('',#15875,#3666);
#2514=LINE('',#15876,#3667);
#2515=LINE('',#15879,#3668);
#2516=LINE('',#15881,#3669);
#2517=LINE('',#15882,#3670);
#2518=LINE('',#15885,#3671);
#2519=LINE('',#15887,#3672);
#2520=LINE('',#15888,#3673);
#2521=LINE('',#15891,#3674);
#2522=LINE('',#15893,#3675);
#2523=LINE('',#15894,#3676);
#2524=LINE('',#15896,#3677);
#2525=LINE('',#15897,#3678);
#2526=LINE('',#15907,#3679);
#2527=LINE('',#15911,#3680);
#3661=VECTOR('',#12819,1.);
#3662=VECTOR('',#12820,1.);
#3663=VECTOR('',#12821,1.);
#3664=VECTOR('',#12822,1.);
#3665=VECTOR('',#12825,1.);
#3666=VECTOR('',#12826,1.);
#3667=VECTOR('',#12827,1.);
#3668=VECTOR('',#12830,1.);
#3669=VECTOR('',#12831,1.);
#3670=VECTOR('',#12832,1.);
#3671=VECTOR('',#12835,1.);
#3672=VECTOR('',#12836,1.);
#3673=VECTOR('',#12837,1.);
#3674=VECTOR('',#12840,1.);
#3675=VECTOR('',#12841,1.);
#3676=VECTOR('',#12842,1.);
#3677=VECTOR('',#12845,1.);
#3678=VECTOR('',#12846,1.);
#3679=VECTOR('',#12859,0.275);
#3680=VECTOR('',#12864,0.15);
#4743=CIRCLE('',#11553,0.275);
#4744=CIRCLE('',#11554,0.15);
#4745=CIRCLE('',#11556,0.275);
#4746=CIRCLE('',#11559,0.15);
#5073=VERTEX_POINT('',#15863);
#5074=VERTEX_POINT('',#15864);
#5075=VERTEX_POINT('',#15866);
#5076=VERTEX_POINT('',#15868);
#5077=VERTEX_POINT('',#15872);
#5078=VERTEX_POINT('',#15874);
#5079=VERTEX_POINT('',#15878);
#5080=VERTEX_POINT('',#15880);
#5081=VERTEX_POINT('',#15884);
#5082=VERTEX_POINT('',#15886);
#5083=VERTEX_POINT('',#15890);
#5084=VERTEX_POINT('',#15892);
#5085=VERTEX_POINT('',#15900);
#5086=VERTEX_POINT('',#15902);
#5087=VERTEX_POINT('',#15905);
#5088=VERTEX_POINT('',#15910);
#6079=EDGE_CURVE('',#5073,#5074,#2508,.T.);
#6080=EDGE_CURVE('',#5075,#5073,#2509,.T.);
#6081=EDGE_CURVE('',#5075,#5076,#2510,.T.);
#6082=EDGE_CURVE('',#5076,#5074,#2511,.T.);
#6083=EDGE_CURVE('',#5074,#5077,#2512,.T.);
#6084=EDGE_CURVE('',#5076,#5078,#2513,.T.);
#6085=EDGE_CURVE('',#5078,#5077,#2514,.T.);
#6086=EDGE_CURVE('',#5077,#5079,#2515,.T.);
#6087=EDGE_CURVE('',#5078,#5080,#2516,.T.);
#6088=EDGE_CURVE('',#5080,#5079,#2517,.T.);
#6089=EDGE_CURVE('',#5079,#5081,#2518,.T.);
#6090=EDGE_CURVE('',#5080,#5082,#2519,.T.);
#6091=EDGE_CURVE('',#5082,#5081,#2520,.T.);
#6092=EDGE_CURVE('',#5081,#5083,#2521,.T.);
#6093=EDGE_CURVE('',#5082,#5084,#2522,.T.);
#6094=EDGE_CURVE('',#5084,#5083,#2523,.T.);
#6095=EDGE_CURVE('',#5083,#5073,#2524,.T.);
#6096=EDGE_CURVE('',#5084,#5075,#2525,.T.);
#6097=EDGE_CURVE('',#5085,#5085,#4743,.T.);
#6098=EDGE_CURVE('',#5086,#5086,#4744,.T.);
#6099=EDGE_CURVE('',#5087,#5087,#4745,.T.);
#6100=EDGE_CURVE('',#5087,#5085,#2526,.T.);
#6101=EDGE_CURVE('',#5086,#5088,#2527,.T.);
#6102=EDGE_CURVE('',#5088,#5088,#4746,.T.);
#7736=ORIENTED_EDGE('',*,*,#6079,.F.);
#7737=ORIENTED_EDGE('',*,*,#6080,.F.);
#7738=ORIENTED_EDGE('',*,*,#6081,.T.);
#7739=ORIENTED_EDGE('',*,*,#6082,.T.);
#7740=ORIENTED_EDGE('',*,*,#6083,.F.);
#7741=ORIENTED_EDGE('',*,*,#6082,.F.);
#7742=ORIENTED_EDGE('',*,*,#6084,.T.);
#7743=ORIENTED_EDGE('',*,*,#6085,.T.);
#7744=ORIENTED_EDGE('',*,*,#6086,.F.);
#7745=ORIENTED_EDGE('',*,*,#6085,.F.);
#7746=ORIENTED_EDGE('',*,*,#6087,.T.);
#7747=ORIENTED_EDGE('',*,*,#6088,.T.);
#7748=ORIENTED_EDGE('',*,*,#6089,.F.);
#7749=ORIENTED_EDGE('',*,*,#6088,.F.);
#7750=ORIENTED_EDGE('',*,*,#6090,.T.);
#7751=ORIENTED_EDGE('',*,*,#6091,.T.);
#7752=ORIENTED_EDGE('',*,*,#6092,.F.);
#7753=ORIENTED_EDGE('',*,*,#6091,.F.);
#7754=ORIENTED_EDGE('',*,*,#6093,.T.);
#7755=ORIENTED_EDGE('',*,*,#6094,.T.);
#7756=ORIENTED_EDGE('',*,*,#6095,.F.);
#7757=ORIENTED_EDGE('',*,*,#6094,.F.);
#7758=ORIENTED_EDGE('',*,*,#6096,.T.);
#7759=ORIENTED_EDGE('',*,*,#6080,.T.);
#7760=ORIENTED_EDGE('',*,*,#6087,.F.);
#7761=ORIENTED_EDGE('',*,*,#6084,.F.);
#7762=ORIENTED_EDGE('',*,*,#6081,.F.);
#7763=ORIENTED_EDGE('',*,*,#6096,.F.);
#7764=ORIENTED_EDGE('',*,*,#6093,.F.);
#7765=ORIENTED_EDGE('',*,*,#6090,.F.);
#7766=ORIENTED_EDGE('',*,*,#6097,.F.);
#7767=ORIENTED_EDGE('',*,*,#6098,.T.);
#7768=ORIENTED_EDGE('',*,*,#6099,.F.);
#7769=ORIENTED_EDGE('',*,*,#6100,.T.);
#7770=ORIENTED_EDGE('',*,*,#6097,.T.);
#7771=ORIENTED_EDGE('',*,*,#6100,.F.);
#7772=ORIENTED_EDGE('',*,*,#6099,.T.);
#7773=ORIENTED_EDGE('',*,*,#6089,.T.);
#7774=ORIENTED_EDGE('',*,*,#6092,.T.);
#7775=ORIENTED_EDGE('',*,*,#6095,.T.);
#7776=ORIENTED_EDGE('',*,*,#6079,.T.);
#7777=ORIENTED_EDGE('',*,*,#6083,.T.);
#7778=ORIENTED_EDGE('',*,*,#6086,.T.);
#7779=ORIENTED_EDGE('',*,*,#6098,.F.);
#7780=ORIENTED_EDGE('',*,*,#6101,.T.);
#7781=ORIENTED_EDGE('',*,*,#6102,.T.);
#7782=ORIENTED_EDGE('',*,*,#6101,.F.);
#7783=ORIENTED_EDGE('',*,*,#6102,.F.);
#10301=CYLINDRICAL_SURFACE('',#11555,0.275);
#10302=CYLINDRICAL_SURFACE('',#11558,0.15);
#10460=ADVANCED_FACE('',(#1118),#581,.F.);
#10461=ADVANCED_FACE('',(#1119),#582,.F.);
#10462=ADVANCED_FACE('',(#1120),#583,.F.);
#10463=ADVANCED_FACE('',(#1121),#584,.F.);
#10464=ADVANCED_FACE('',(#1122),#585,.F.);
#10465=ADVANCED_FACE('',(#1123),#586,.F.);
#10466=ADVANCED_FACE('',(#1124),#587,.T.);
#10467=ADVANCED_FACE('',(#1125,#448),#588,.F.);
#10468=ADVANCED_FACE('',(#1126),#10301,.T.);
#10469=ADVANCED_FACE('',(#1127,#449),#589,.T.);
#10470=ADVANCED_FACE('',(#1128),#10302,.T.);
#10471=ADVANCED_FACE('',(#1129),#590,.F.);
#10995=CLOSED_SHELL('',(#10460,#10461,#10462,#10463,#10464,#10465,#10466,
#10467,#10468,#10469,#10470,#10471));
#11544=AXIS2_PLACEMENT_3D('',#15861,#12815,#12816);
#11545=AXIS2_PLACEMENT_3D('',#15862,#12817,#12818);
#11546=AXIS2_PLACEMENT_3D('',#15871,#12823,#12824);
#11547=AXIS2_PLACEMENT_3D('',#15877,#12828,#12829);
#11548=AXIS2_PLACEMENT_3D('',#15883,#12833,#12834);
#11549=AXIS2_PLACEMENT_3D('',#15889,#12838,#12839);
#11550=AXIS2_PLACEMENT_3D('',#15895,#12843,#12844);
#11551=AXIS2_PLACEMENT_3D('',#15898,#12847,#12848);
#11552=AXIS2_PLACEMENT_3D('',#15899,#12849,#12850);
#11553=AXIS2_PLACEMENT_3D('',#15901,#12851,#12852);
#11554=AXIS2_PLACEMENT_3D('',#15903,#12853,#12854);
#11555=AXIS2_PLACEMENT_3D('',#15904,#12855,#12856);
#11556=AXIS2_PLACEMENT_3D('',#15906,#12857,#12858);
#11557=AXIS2_PLACEMENT_3D('',#15908,#12860,#12861);
#11558=AXIS2_PLACEMENT_3D('',#15909,#12862,#12863);
#11559=AXIS2_PLACEMENT_3D('',#15912,#12865,#12866);
#11560=AXIS2_PLACEMENT_3D('',#15913,#12867,#12868);
#12815=DIRECTION('axis',(0.,0.,1.));
#12816=DIRECTION('refdir',(1.,0.,0.));
#12817=DIRECTION('center_axis',(-0.866025403784439,0.,0.499999999999999));
#12818=DIRECTION('ref_axis',(0.499999999999999,0.,0.866025403784439));
#12819=DIRECTION('',(-0.499999999999999,0.,-0.866025403784439));
#12820=DIRECTION('',(0.,1.,0.));
#12821=DIRECTION('',(-0.499999999999999,0.,-0.866025403784439));
#12822=DIRECTION('',(0.,1.,0.));
#12823=DIRECTION('center_axis',(-0.86602540378444,0.,-0.499999999999998));
#12824=DIRECTION('ref_axis',(-0.499999999999998,0.,0.86602540378444));
#12825=DIRECTION('',(0.499999999999998,0.,-0.86602540378444));
#12826=DIRECTION('',(0.499999999999998,0.,-0.86602540378444));
#12827=DIRECTION('',(0.,1.,0.));
#12828=DIRECTION('center_axis',(0.,0.,-1.));
#12829=DIRECTION('ref_axis',(-1.,0.,0.));
#12830=DIRECTION('',(1.,0.,0.));
#12831=DIRECTION('',(1.,0.,0.));
#12832=DIRECTION('',(0.,1.,0.));
#12833=DIRECTION('center_axis',(0.866025403784438,0.,-0.5));
#12834=DIRECTION('ref_axis',(-0.5,0.,-0.866025403784438));
#12835=DIRECTION('',(0.5,0.,0.866025403784438));
#12836=DIRECTION('',(0.5,0.,0.866025403784438));
#12837=DIRECTION('',(0.,1.,0.));
#12838=DIRECTION('center_axis',(0.866025403784438,0.,0.5));
#12839=DIRECTION('ref_axis',(0.5,0.,-0.866025403784438));
#12840=DIRECTION('',(-0.5,0.,0.866025403784438));
#12841=DIRECTION('',(-0.5,0.,0.866025403784438));
#12842=DIRECTION('',(0.,1.,0.));
#12843=DIRECTION('center_axis',(0.,0.,1.));
#12844=DIRECTION('ref_axis',(1.,0.,0.));
#12845=DIRECTION('',(-1.,0.,0.));
#12846=DIRECTION('',(-1.,0.,0.));
#12847=DIRECTION('center_axis',(0.,1.,0.));
#12848=DIRECTION('ref_axis',(1.,0.,0.));
#12849=DIRECTION('center_axis',(0.,1.,0.));
#12850=DIRECTION('ref_axis',(1.,0.,0.));
#12851=DIRECTION('center_axis',(0.,1.,0.));
#12852=DIRECTION('ref_axis',(1.,0.,0.));
#12853=DIRECTION('center_axis',(0.,1.,0.));
#12854=DIRECTION('ref_axis',(1.,0.,0.));
#12855=DIRECTION('center_axis',(0.,1.,0.));
#12856=DIRECTION('ref_axis',(1.,0.,0.));
#12857=DIRECTION('center_axis',(0.,1.,0.));
#12858=DIRECTION('ref_axis',(1.,0.,0.));
#12859=DIRECTION('',(0.,-1.,0.));
#12860=DIRECTION('center_axis',(0.,1.,0.));
#12861=DIRECTION('ref_axis',(1.,0.,0.));
#12862=DIRECTION('center_axis',(0.,1.,0.));
#12863=DIRECTION('ref_axis',(1.,0.,0.));
#12864=DIRECTION('',(0.,-1.,0.));
#12865=DIRECTION('center_axis',(0.,1.,0.));
#12866=DIRECTION('ref_axis',(1.,0.,0.));
#12867=DIRECTION('center_axis',(0.,1.,0.));
#12868=DIRECTION('ref_axis',(1.,0.,0.));
#15861=CARTESIAN_POINT('',(0.,0.,0.));
#15862=CARTESIAN_POINT('Origin',(1.40566243270259,-6.9,2.67));
#15863=CARTESIAN_POINT('',(1.4778312163513,-6.7,2.795));
#15864=CARTESIAN_POINT('',(1.40566243270259,-6.7,2.67));
#15865=CARTESIAN_POINT('',(1.42370462861477,-6.7,2.70125));
#15866=CARTESIAN_POINT('',(1.4778312163513,-6.9,2.795));
#15867=CARTESIAN_POINT('',(1.4778312163513,-6.9,2.795));
#15868=CARTESIAN_POINT('',(1.40566243270259,-6.9,2.67));
#15869=CARTESIAN_POINT('',(1.4778312163513,-6.9,2.795));
#15870=CARTESIAN_POINT('',(1.40566243270259,-6.9,2.67));
#15871=CARTESIAN_POINT('Origin',(1.4778312163513,-6.9,2.545));
#15872=CARTESIAN_POINT('',(1.4778312163513,-6.7,2.545));
#15873=CARTESIAN_POINT('',(1.45978902043912,-6.7,2.57625));
#15874=CARTESIAN_POINT('',(1.4778312163513,-6.9,2.545));
#15875=CARTESIAN_POINT('',(1.40566243270259,-6.9,2.67));
#15876=CARTESIAN_POINT('',(1.4778312163513,-6.9,2.545));
#15877=CARTESIAN_POINT('Origin',(1.6221687836487,-6.9,2.545));
#15878=CARTESIAN_POINT('',(1.6221687836487,-6.7,2.545));
#15879=CARTESIAN_POINT('',(1.58608439182435,-6.7,2.545));
#15880=CARTESIAN_POINT('',(1.6221687836487,-6.9,2.545));
#15881=CARTESIAN_POINT('',(1.4778312163513,-6.9,2.545));
#15882=CARTESIAN_POINT('',(1.6221687836487,-6.9,2.545));
#15883=CARTESIAN_POINT('Origin',(1.69433756729741,-6.9,2.67));
#15884=CARTESIAN_POINT('',(1.69433756729741,-6.7,2.67));
#15885=CARTESIAN_POINT('',(1.67629537138523,-6.7,2.63875));
#15886=CARTESIAN_POINT('',(1.69433756729741,-6.9,2.67));
#15887=CARTESIAN_POINT('',(1.6221687836487,-6.9,2.545));
#15888=CARTESIAN_POINT('',(1.69433756729741,-6.9,2.67));
#15889=CARTESIAN_POINT('Origin',(1.6221687836487,-6.9,2.795));
#15890=CARTESIAN_POINT('',(1.6221687836487,-6.7,2.795));
#15891=CARTESIAN_POINT('',(1.64021097956088,-6.7,2.76375));
#15892=CARTESIAN_POINT('',(1.6221687836487,-6.9,2.795));
#15893=CARTESIAN_POINT('',(1.69433756729741,-6.9,2.67));
#15894=CARTESIAN_POINT('',(1.6221687836487,-6.9,2.795));
#15895=CARTESIAN_POINT('Origin',(1.4778312163513,-6.9,2.795));
#15896=CARTESIAN_POINT('',(1.51391560817565,-6.7,2.795));
#15897=CARTESIAN_POINT('',(1.6221687836487,-6.9,2.795));
#15898=CARTESIAN_POINT('Origin',(1.55,-6.9,2.67));
#15899=CARTESIAN_POINT('Origin',(1.55,-7.,2.67));
#15900=CARTESIAN_POINT('',(1.275,-7.,2.67));
#15901=CARTESIAN_POINT('Origin',(1.55,-7.,2.67));
#15902=CARTESIAN_POINT('',(1.4,-7.,2.67));
#15903=CARTESIAN_POINT('Origin',(1.55,-7.,2.67));
#15904=CARTESIAN_POINT('Origin',(1.55,-7.,2.67));
#15905=CARTESIAN_POINT('',(1.275,-6.7,2.67));
#15906=CARTESIAN_POINT('Origin',(1.55,-6.7,2.67));
#15907=CARTESIAN_POINT('',(1.275,-7.,2.67));
#15908=CARTESIAN_POINT('Origin',(1.55,-6.7,2.67));
#15909=CARTESIAN_POINT('Origin',(1.55,-8.,2.67));
#15910=CARTESIAN_POINT('',(1.4,-8.,2.67));
#15911=CARTESIAN_POINT('',(1.4,-8.,2.67));
#15912=CARTESIAN_POINT('Origin',(1.55,-8.,2.67));
#15913=CARTESIAN_POINT('Origin',(1.55,-8.,2.67));
#19299=UNCERTAINTY_MEASURE_WITH_UNIT(LENGTH_MEASURE(0.001),#19362,
'DISTANCE_ACCURACY_VALUE',
'Maximum model space distance between geometric entities at asserted c
onnectivities');
#19323=UNCERTAINTY_MEASURE_WITH_UNIT(LENGTH_MEASURE(0.001),#19362,
'DISTANCE_ACCURACY_VALUE',
'Maximum model space distance between geometric entities at asserted c
onnectivities');
#19337=(
GEOMETRIC_REPRESENTATION_CONTEXT(3)
GLOBAL_UNCERTAINTY_ASSIGNED_CONTEXT((#19299))
GLOBAL_UNIT_ASSIGNED_CONTEXT((#19362,#19364,#19365))
REPRESENTATION_CONTEXT('','3D')
);
#19361=(
GEOMETRIC_REPRESENTATION_CONTEXT(3)
GLOBAL_UNCERTAINTY_ASSIGNED_CONTEXT((#19323))
GLOBAL_UNIT_ASSIGNED_CONTEXT((#19362,#19364,#19365))
REPRESENTATION_CONTEXT('','3D')
);
#19362=(
LENGTH_UNIT()
NAMED_UNIT(*)
SI_UNIT(.CENTI.,.METRE.)
);
#19364=(
NAMED_UNIT(*)
PLANE_ANGLE_UNIT()
SI_UNIT($,.RADIAN.)
);
#19365=(
NAMED_UNIT(*)
SI_UNIT($,.STERADIAN.)
SOLID_ANGLE_UNIT()
);
#19379=SHAPE_DEFINITION_REPRESENTATION(#19416,#19501);
#19416=PRODUCT_DEFINITION_SHAPE('',$,#19539);
#19501=SHAPE_REPRESENTATION('',(#11544),#19337);
#19525=PRODUCT_DEFINITION_CONTEXT('part definition',#19638,'design');
#19539=PRODUCT_DEFINITION('M3x10 motor screw (2)','M3x10 motor screw (2)',
#19576,#19525);
#19576=PRODUCT_DEFINITION_FORMATION('',$,#19653);
#19638=APPLICATION_CONTEXT(
'Core Data for Automotive Mechanical Design Process');
#19639=PRODUCT_CONTEXT('part definition',#19638,'mechanical');
#19653=PRODUCT('M3x10 motor screw (2)','M3x10 motor screw (2)',
'M3x10 motor screw (2)',(#19639));
#19747=COLOUR_RGB('Black',0.12,0.14,0.17);
#19748=FILL_AREA_STYLE_COLOUR('',#19747);
#19749=FILL_AREA_STYLE('',(#19748));
#19750=SURFACE_STYLE_FILL_AREA(#19749);
#19751=SURFACE_SIDE_STYLE('',(#19750));
#19752=SURFACE_STYLE_USAGE(.BOTH.,#19751);
#19753=PRESENTATION_STYLE_ASSIGNMENT((#19752));
ENDSEC;
END-ISO-10303-21;
